ISO-10303-21;
HEADER;
FILE_DESCRIPTION (('STEP AP214'),
    '1' );
FILE_NAME ('Cap Screw.step',
    '2026-10-23T18:01:19',
    ( '' ),
    ( '' ),
    'SwSTEP 2.0',
    'SolidWorks 2025',
    '' );
FILE_SCHEMA (( 'AUTOMOTIVE_DESIGN' ));
ENDSEC;

DATA;
#3=CARTESIAN_POINT ( 'NONE',  ( 0.000000000000000000, 0.03800000000000004763, 0.000000000000000000 ) ) ;
#48=CARTESIAN_POINT ( 'NONE',  ( -0.09035531712817639061, 1.379999999999999671, 0.1565000000000000280 ) ) ;
#139=LINE ( 'NONE', #8292, #12561 ) ;
#189=ORIENTED_EDGE ( 'NONE', *, *, #6062, .T. ) ;
#209=DIRECTION ( 'NONE',  ( 0.000000000000000000, 0.000000000000000000, 1.000000000000000000 ) ) ;
#219=ADVANCED_FACE ( 'NONE', ( #3751 ), #1356, .F. ) ;
#272=DIRECTION ( 'NONE',  ( -0.000000000000000000, -1.000000000000000000, -0.000000000000000000 ) ) ;
#280=CARTESIAN_POINT ( 'NONE',  ( 0.000000000000000000, 1.629999999999999893, 0.000000000000000000 ) ) ;
#308=EDGE_CURVE ( 'NONE', #4201, #2516, #10088, .T. ) ;
#309=VECTOR ( 'NONE', #6967, 39.37007874015748143 ) ;
#333=AXIS2_PLACEMENT_3D ( 'NONE', #4078, #9892, #14552 ) ;
#343=EDGE_CURVE ( 'NONE', #4313, #8918, #8861, .T. ) ;
#348=DIRECTION ( 'NONE',  ( 0.8660254037844387076, 0.000000000000000000, 0.4999999999999999445 ) ) ;
#365=EDGE_CURVE ( 'NONE', #9131, #9822, #10086, .T. ) ;
#381=AXIS2_PLACEMENT_3D ( 'NONE', #11771, #13044, #15132 ) ;
#417=DIRECTION ( 'NONE',  ( -0.000000000000000000, -1.000000000000000000, -0.000000000000000000 ) ) ;
#438=CARTESIAN_POINT ( 'NONE',  ( 0.000000000000000000, 1.249999999999999778, 0.000000000000000000 ) ) ;
#494=CARTESIAN_POINT ( 'NONE',  ( 0.09035531712817643224, 1.379999999999999671, 0.1564999999999999447 ) ) ;
#533=LINE ( 'NONE', #9820, #5247 ) ;
#554=DIRECTION ( 'NONE',  ( 0.000000000000000000, 0.000000000000000000, 1.000000000000000000 ) ) ;
#599=ORIENTED_EDGE ( 'NONE', *, *, #9243, .T. ) ;
#662=CARTESIAN_POINT ( 'NONE',  ( 0.000000000000000000, 1.591999999999999638, -0.2812500000000000555 ) ) ;
#686=AXIS2_PLACEMENT_3D ( 'NONE', #12659, #6869, #8926 ) ;
#688=AXIS2_PLACEMENT_3D ( 'NONE', #8760, #9762, #10906 ) ;
#712=ORIENTED_EDGE ( 'NONE', *, *, #4651, .T. ) ;
#722=EDGE_CURVE ( 'NONE', #5214, #9310, #5440, .T. ) ;
#734=CARTESIAN_POINT ( 'NONE',  ( 0.000000000000000000, 1.629999999999999893, 0.000000000000000000 ) ) ;
#865=DIRECTION ( 'NONE',  ( -0.000000000000000000, -1.000000000000000000, -0.000000000000000000 ) ) ;
#866=FACE_OUTER_BOUND ( 'NONE', #10958, .T. ) ;
#873=CIRCLE ( 'NONE', #14568, 0.2432499999999999385 ) ;
#913=DIRECTION ( 'NONE',  ( 0.000000000000000000, 0.000000000000000000, 1.000000000000000000 ) ) ;
#925=CARTESIAN_POINT ( 'NONE',  ( 0.1807106342563528367, 1.379999999999999671, 5.178337979384803075E-18 ) ) ;
#929=CARTESIAN_POINT ( 'NONE',  ( 0.09035531712817648775, 1.629999999999999893, -0.1564999999999998892 ) ) ;
#945=UNCERTAINTY_MEASURE_WITH_UNIT (LENGTH_MEASURE( 1.000000000000000082E-05 ), #5734, 'distance_accuracy_value', 'NONE');
#963=CARTESIAN_POINT ( 'NONE',  ( 3.211636230763933762E-17, 1.629999999999999893, 0.2432499999999999385 ) ) ;
#986=FACE_OUTER_BOUND ( 'NONE', #13920, .T. ) ;
#1017=VERTEX_POINT ( 'NONE', #3681 ) ;
#1075=ORIENTED_EDGE ( 'NONE', *, *, #4649, .F. ) ;
#1095=PRODUCT_DEFINITION_CONTEXT ( 'detailed design', #1849, 'design' ) ;
#1122=CARTESIAN_POINT ( 'NONE',  ( 0.09035531712817643224, 1.379999999999999671, 0.1564999999999999447 ) ) ;
#1123=LENGTH_MEASURE_WITH_UNIT ( LENGTH_MEASURE( 0.02539999999999999897 ), #3281 );
#1136=EDGE_CURVE ( 'NONE', #14886, #5214, #8635, .T. ) ;
#1137=ORIENTED_EDGE ( 'NONE', *, *, #12490, .F. ) ;
#1182=EDGE_CURVE ( 'NONE', #6882, #11005, #9441, .T. ) ;
#1205=CARTESIAN_POINT ( 'NONE',  ( -0.09035531712817639061, 1.379999999999999671, -0.1564999999999998892 ) ) ;
#1222=DIRECTION ( 'NONE',  ( 0.000000000000000000, 0.000000000000000000, -1.000000000000000000 ) ) ;
#1241=CARTESIAN_POINT ( 'NONE',  ( 0.09035531712817648775, 1.379999999999999671, -0.1564999999999998892 ) ) ;
#1273=CYLINDRICAL_SURFACE ( 'NONE', #11108, 0.2812500000000000555 ) ;
#1298=AXIS2_PLACEMENT_3D ( 'NONE', #9493, #12988, #14142 ) ;
#1311=EDGE_CURVE ( 'NONE', #11971, #13813, #11437, .T. ) ;
#1325=LINE ( 'NONE', #1403, #3569 ) ;
#1327=CARTESIAN_POINT ( 'NONE',  ( 3.444319122601930972E-17, 1.591999999999999638, 0.2812500000000000555 ) ) ;
#1356=PLANE ( 'NONE',  #4864 ) ;
#1370=ORIENTED_EDGE ( 'NONE', *, *, #14359, .F. ) ;
#1380=AXIS2_PLACEMENT_3D ( 'NONE', #8031, #11306, #6581 ) ;
#1403=CARTESIAN_POINT ( 'NONE',  ( 0.000000000000000000, 0.000000000000000000, -0.1900000000000000577 ) ) ;
#1418=ORIENTED_EDGE ( 'NONE', *, *, #8906, .F. ) ;
#1435=VECTOR ( 'NONE', #12984, 39.37007874015748143 ) ;
#1451=EDGE_LOOP ( 'NONE', ( #10714, #8361, #4810, #7280 ) ) ;
#1458=ORIENTED_EDGE ( 'NONE', *, *, #8228, .F. ) ;
#1464=ADVANCED_FACE ( 'NONE', ( #14693 ), #13750, .T. ) ;
#1472=PLANE ( 'NONE',  #7765 ) ;
#1498=DIRECTION ( 'NONE',  ( -0.000000000000000000, -1.000000000000000000, -0.000000000000000000 ) ) ;
#1521=DIRECTION ( 'NONE',  ( 1.000000000000000000, 0.000000000000000000, 0.000000000000000000 ) ) ;
#1523=EDGE_LOOP ( 'NONE', ( #7284, #1075, #6871, #10896 ) ) ;
#1538=ORIENTED_EDGE ( 'NONE', *, *, #4649, .T. ) ;
#1564=FACE_OUTER_BOUND ( 'NONE', #4686, .T. ) ;
#1567=VECTOR ( 'NONE', #10993, 39.37007874015748854 ) ;
#1569=PLANE ( 'NONE',  #5999 ) ;
#1611=AXIS2_PLACEMENT_3D ( 'NONE', #10243, #11382, #12675 ) ;
#1644=AXIS2_PLACEMENT_3D ( 'NONE', #2005, #3182, #10362 ) ;
#1682=MECHANICAL_DESIGN_GEOMETRIC_PRESENTATION_REPRESENTATION('',(#13406),#9532);
#1737=ORIENTED_EDGE ( 'NONE', *, *, #7176, .T. ) ;
#1739=VECTOR ( 'NONE', #1939, 39.37007874015748143 ) ;
#1762=ADVANCED_FACE ( 'NONE', ( #13099 ), #9748, .T. ) ;
#1764=PLANE ( 'NONE',  #9015 ) ;
#1838=( NAMED_UNIT ( * ) PLANE_ANGLE_UNIT ( ) SI_UNIT ( $, .RADIAN. ) );
#1849=APPLICATION_CONTEXT ( 'automotive_design' ) ;
#1863=VECTOR ( 'NONE', #12907, 39.37007874015748854 ) ;
#1899=CARTESIAN_POINT ( 'NONE',  ( 0.1807106342563528367, 1.629999999999999893, 5.178337979384803075E-18 ) ) ;
#1916=( LENGTH_UNIT ( ) NAMED_UNIT ( * ) SI_UNIT ( $, .METRE. ) );
#1928=ADVANCED_FACE ( 'NONE', ( #7668, #5532 ), #1764, .T. ) ;
#1939=DIRECTION ( 'NONE',  ( -0.000000000000000000, -1.000000000000000000, -0.000000000000000000 ) ) ;
#2005=CARTESIAN_POINT ( 'NONE',  ( 0.000000000000000000, 1.249999999999999778, 0.000000000000000000 ) ) ;
#2020=PLANE ( 'NONE',  #686 ) ;
#2037=ORIENTED_EDGE ( 'NONE', *, *, #11368, .F. ) ;
#2085=CONICAL_SURFACE ( 'NONE', #4310, 0.2812500000000000555, 0.7853981633974465026 ) ;
#2142=DIRECTION ( 'NONE',  ( 0.000000000000000000, 0.000000000000000000, -1.000000000000000000 ) ) ;
#2185=DIRECTION ( 'NONE',  ( 0.000000000000000000, 0.000000000000000000, -1.000000000000000000 ) ) ;
#2231=EDGE_CURVE ( 'NONE', #9631, #11384, #11873, .T. ) ;
#2274=ORIENTED_EDGE ( 'NONE', *, *, #14689, .T. ) ;
#2301=DIRECTION ( 'NONE',  ( 0.000000000000000000, 0.000000000000000000, 1.000000000000000000 ) ) ;
#2320=CIRCLE ( 'NONE', #6720, 0.2812500000000000555 ) ;
#2355=ORIENTED_EDGE ( 'NONE', *, *, #5210, .F. ) ;
#2356=LINE ( 'NONE', #6032, #10422 ) ;
#2386=VECTOR ( 'NONE', #6238, 39.37007874015748143 ) ;
#2412=ORIENTED_EDGE ( 'NONE', *, *, #9018, .F. ) ;
#2414=AXIS2_PLACEMENT_3D ( 'NONE', #8588, #6144, #14390 ) ;
#2415=EDGE_LOOP ( 'NONE', ( #3462, #6075, #12152, #11692 ) ) ;
#2437=ORIENTED_EDGE ( 'NONE', *, *, #7129, .T. ) ;
#2479=CARTESIAN_POINT ( 'NONE',  ( 0.09035531712817643224, 1.379999999999999671, 0.1564999999999999447 ) ) ;
#2485=PRODUCT_DEFINITION ( 'UNKNOWN', '', #3289, #1095 ) ;
#2490=UNCERTAINTY_MEASURE_WITH_UNIT (LENGTH_MEASURE( 1.000000000000000082E-05 ), #14703, 'distance_accuracy_value', 'NONE');
#2516=VERTEX_POINT ( 'NONE', #3750 ) ;
#2536=VERTEX_POINT ( 'NONE', #7486 ) ;
#2551=DIRECTION ( 'NONE',  ( -0.000000000000000000, 1.000000000000000000, -0.000000000000000000 ) ) ;
#2571=ADVANCED_FACE ( 'NONE', ( #6192 ), #2085, .T. ) ;
#2598=PLANE ( 'NONE',  #1298 ) ;
#2600=EDGE_CURVE ( 'NONE', #2516, #4201, #5523, .T. ) ;
#2649=AXIS2_PLACEMENT_3D ( 'NONE', #14520, #6365, #11083 ) ;
#2672=FACE_OUTER_BOUND ( 'NONE', #1523, .T. ) ;
#2695=VECTOR ( 'NONE', #417, 39.37007874015748143 ) ;
#2732=ORIENTED_EDGE ( 'NONE', *, *, #6388, .F. ) ;
#2744=DIRECTION ( 'NONE',  ( -0.000000000000000000, -1.000000000000000000, -0.000000000000000000 ) ) ;
#2755=ORIENTED_EDGE ( 'NONE', *, *, #6528, .T. ) ;
#2784=CARTESIAN_POINT ( 'NONE',  ( 3.444319122601930972E-17, 1.249999999999999778, 0.2812500000000000555 ) ) ;
#2796=VECTOR ( 'NONE', #8805, 39.37007874015748143 ) ;
#2802=VECTOR ( 'NONE', #11427, 39.37007874015748143 ) ;
#2832=ORIENTED_EDGE ( 'NONE', *, *, #6418, .T. ) ;
#2912=EDGE_CURVE ( 'NONE', #8918, #3698, #533, .T. ) ;
#2940=ORIENTED_EDGE ( 'NONE', *, *, #5610, .F. ) ;
#2942=VERTEX_POINT ( 'NONE', #2784 ) ;
#2961=ADVANCED_FACE ( 'NONE', ( #7385 ), #3935, .T. ) ;
#3039=DIRECTION ( 'NONE',  ( -0.5000000000000000000, 0.000000000000000000, 0.8660254037844385966 ) ) ;
#3125=CARTESIAN_POINT ( 'NONE',  ( 0.000000000000000000, 1.159999999999999698, 0.000000000000000000 ) ) ;
#3154=CARTESIAN_POINT ( 'NONE',  ( 0.000000000000000000, 1.249999999999999778, -0.3190000000000000058 ) ) ;
#3182=DIRECTION ( 'NONE',  ( -0.000000000000000000, -1.000000000000000000, -0.000000000000000000 ) ) ;
#3278=( GEOMETRIC_REPRESENTATION_CONTEXT ( 3 ) GLOBAL_UNCERTAINTY_ASSIGNED_CONTEXT ( ( #945 ) ) GLOBAL_UNIT_ASSIGNED_CONTEXT ( ( #5734, #11774, #6807 ) ) REPRESENTATION_CONTEXT ( 'NONE', 'WORKASPACE' ) );
#3281=( LENGTH_UNIT ( ) NAMED_UNIT ( * ) SI_UNIT ( $, .METRE. ) );
#3289=PRODUCT_DEFINITION_FORMATION_WITH_SPECIFIED_SOURCE ( 'ANY', '', #12392, .NOT_KNOWN. ) ;
#3292=DIRECTION ( 'NONE',  ( 0.000000000000000000, -1.000000000000000000, -0.000000000000000000 ) ) ;
#3294=LINE ( 'NONE', #12465, #13271 ) ;
#3333=CYLINDRICAL_SURFACE ( 'NONE', #11161, 0.2812500000000000555 ) ;
#3365=CIRCLE ( 'NONE', #1644, 0.3190000000000000058 ) ;
#3394=LINE ( 'NONE', #10280, #8880 ) ;
#3401=EDGE_CURVE ( 'NONE', #11384, #3698, #8383, .T. ) ;
#3404=CONICAL_SURFACE ( 'NONE', #11711, 0.2812500000000000555, 0.7853981633974465026 ) ;
#3427=ORIENTED_EDGE ( 'NONE', *, *, #365, .F. ) ;
#3433=DIRECTION ( 'NONE',  ( 0.000000000000000000, -0.000000000000000000, 1.000000000000000000 ) ) ;
#3457=FACE_OUTER_BOUND ( 'NONE', #12822, .T. ) ;
#3462=ORIENTED_EDGE ( 'NONE', *, *, #12529, .F. ) ;
#3487=AXIS2_PLACEMENT_3D ( 'NONE', #7031, #12669, #13809 ) ;
#3529=CYLINDRICAL_SURFACE ( 'NONE', #4995, 0.3190000000000000058 ) ;
#3569=VECTOR ( 'NONE', #12961, 39.37007874015748143 ) ;
#3614=DIRECTION ( 'NONE',  ( 0.000000000000000000, 0.000000000000000000, -1.000000000000000000 ) ) ;
#3661=CONICAL_SURFACE ( 'NONE', #688, 0.1520000000000001905, 0.7853981633974460586 ) ;
#3681=CARTESIAN_POINT ( 'NONE',  ( 0.09035531712817648775, 1.379999999999999671, -0.1564999999999998892 ) ) ;
#3698=VERTEX_POINT ( 'NONE', #7193 ) ;
#3721=CARTESIAN_POINT ( 'NONE',  ( -0.1807106342563527812, 1.379999999999999671, 3.262375646219079751E-17 ) ) ;
#3750=CARTESIAN_POINT ( 'NONE',  ( 2.326828918379971488E-17, 1.159999999999999698, 0.1899999999999999745 ) ) ;
#3751=FACE_OUTER_BOUND ( 'NONE', #11040, .T. ) ;
#3806=ORIENTED_EDGE ( 'NONE', *, *, #6528, .F. ) ;
#3812=SHAPE_DEFINITION_REPRESENTATION ( #6043, #8297 ) ;
#3885=ORIENTED_EDGE ( 'NONE', *, *, #4468, .F. ) ;
#3907=AXIS2_PLACEMENT_3D ( 'NONE', #7065, #8133, #2301 ) ;
#3935=PLANE ( 'NONE',  #333 ) ;
#3938=DIMENSIONAL_EXPONENTS ( 1.000000000000000000, 0.000000000000000000, 0.000000000000000000, 0.000000000000000000, 0.000000000000000000, 0.000000000000000000, 0.000000000000000000 ) ;
#4032=ORIENTED_EDGE ( 'NONE', *, *, #11368, .T. ) ;
#4040=DIRECTION ( 'NONE',  ( 0.000000000000000000, 0.000000000000000000, -1.000000000000000000 ) ) ;
#4078=CARTESIAN_POINT ( 'NONE',  ( 0.000000000000000000, 1.379999999999999671, 0.000000000000000000 ) ) ;
#4139=LINE ( 'NONE', #11084, #2796 ) ;
#4201=VERTEX_POINT ( 'NONE', #7640 ) ;
#4206=ADVANCED_FACE ( 'NONE', ( #9864 ), #8644, .F. ) ;
#4218=CARTESIAN_POINT ( 'NONE',  ( 0.1900000000000001132, -1.002374524060224757E-18, 0.000000000000000000 ) ) ;
#4233=CARTESIAN_POINT ( 'NONE',  ( 0.000000000000000000, 1.249999999999999778, -0.2812500000000000555 ) ) ;
#4256=ORIENTED_EDGE ( 'NONE', *, *, #6062, .F. ) ;
#4310=AXIS2_PLACEMENT_3D ( 'NONE', #12069, #272, #10851 ) ;
#4313=VERTEX_POINT ( 'NONE', #5580 ) ;
#4383=VECTOR ( 'NONE', #11223, 39.37007874015748143 ) ;
#4395=EDGE_LOOP ( 'NONE', ( #6595, #11723 ) ) ;
#4401=EDGE_CURVE ( 'NONE', #2942, #12302, #13369, .T. ) ;
#4421=ADVANCED_FACE ( 'NONE', ( #9257, #12378 ), #11240, .T. ) ;
#4433=FACE_OUTER_BOUND ( 'NONE', #9451, .T. ) ;
#4468=EDGE_CURVE ( 'NONE', #15151, #5693, #12827, .T. ) ;
#4503=ORIENTED_EDGE ( 'NONE', *, *, #1311, .T. ) ;
#4526=ORIENTED_EDGE ( 'NONE', *, *, #13034, .T. ) ;
#4532=DIRECTION ( 'NONE',  ( -0.000000000000000000, -1.000000000000000000, -0.000000000000000000 ) ) ;
#4564=LINE ( 'NONE', #1327, #7860 ) ;
#4565=CARTESIAN_POINT ( 'NONE',  ( -0.09035531712817639061, 1.379999999999999671, -0.1564999999999998892 ) ) ;
#4649=EDGE_CURVE ( 'NONE', #6882, #8178, #873, .T. ) ;
#4651=EDGE_CURVE ( 'NONE', #14886, #13231, #11403, .T. ) ;
#4686=EDGE_LOOP ( 'NONE', ( #12172, #10059, #13354, #1370 ) ) ;
#4695=DIRECTION ( 'NONE',  ( 0.000000000000000000, 0.000000000000000000, -1.000000000000000000 ) ) ;
#4711=ADVANCED_FACE ( 'NONE', ( #7925 ), #3333, .T. ) ;
#4735=FACE_OUTER_BOUND ( 'NONE', #10209, .T. ) ;
#4810=ORIENTED_EDGE ( 'NONE', *, *, #10945, .F. ) ;
#4817=DIRECTION ( 'NONE',  ( 0.000000000000000000, 0.000000000000000000, -1.000000000000000000 ) ) ;
#4827=AXIS2_PLACEMENT_3D ( 'NONE', #13420, #13121, #6256 ) ;
#4864=AXIS2_PLACEMENT_3D ( 'NONE', #494, #348, #6046 ) ;
#4947=EDGE_CURVE ( 'NONE', #8178, #11602, #4564, .T. ) ;
#4981=AXIS2_PLACEMENT_3D ( 'NONE', #11985, #13040, #12257 ) ;
#4995=AXIS2_PLACEMENT_3D ( 'NONE', #8131, #5911, #2142 ) ;
#5018=ORIENTED_EDGE ( 'NONE', *, *, #4651, .F. ) ;
#5022=AXIS2_PLACEMENT_3D ( 'NONE', #13674, #15059, #13591 ) ;
#5039=DIRECTION ( 'NONE',  ( 0.000000000000000000, 1.000000000000000000, 0.000000000000000000 ) ) ;
#5062=CARTESIAN_POINT ( 'NONE',  ( 0.000000000000000000, 0.000000000000000000, 0.000000000000000000 ) ) ;
#5077=ORIENTED_EDGE ( 'NONE', *, *, #14038, .T. ) ;
#5121=LINE ( 'NONE', #13204, #2695 ) ;
#5130=DIRECTION ( 'NONE',  ( 0.000000000000000000, 1.000000000000000000, 0.000000000000000000 ) ) ;
#5161=EDGE_CURVE ( 'NONE', #11971, #9822, #11120, .T. ) ;
#5210=EDGE_CURVE ( 'NONE', #13813, #9131, #10061, .T. ) ;
#5214=VERTEX_POINT ( 'NONE', #13694 ) ;
#5231=ORIENTED_EDGE ( 'NONE', *, *, #4401, .T. ) ;
#5247=VECTOR ( 'NONE', #11036, 39.37007874015748854 ) ;
#5257=LINE ( 'NONE', #7554, #4383 ) ;
#5285=DIRECTION ( 'NONE',  ( 0.000000000000000000, 0.000000000000000000, -1.000000000000000000 ) ) ;
#5305=DIMENSIONAL_EXPONENTS ( 1.000000000000000000, 0.000000000000000000, 0.000000000000000000, 0.000000000000000000, 0.000000000000000000, 0.000000000000000000, 0.000000000000000000 ) ;
#5357=CARTESIAN_POINT ( 'NONE',  ( -0.09035531712817639061, 1.379999999999999671, -0.1564999999999998892 ) ) ;
#5413=CARTESIAN_POINT ( 'NONE',  ( 3.906623289280057325E-17, 1.159999999999999698, 0.3190000000000000058 ) ) ;
#5432=PLANE ( 'NONE',  #5022 ) ;
#5440=CIRCLE ( 'NONE', #5932, 0.1900000000000000577 ) ;
#5523=CIRCLE ( 'NONE', #13564, 0.1899999999999999745 ) ;
#5532=FACE_OUTER_BOUND ( 'NONE', #11959, .T. ) ;
#5580=CARTESIAN_POINT ( 'NONE',  ( -0.09035531712817639061, 1.629999999999999893, -0.1564999999999998892 ) ) ;
#5590=LINE ( 'NONE', #15064, #309 ) ;
#5610=EDGE_CURVE ( 'NONE', #11384, #15151, #14438, .T. ) ;
#5693=VERTEX_POINT ( 'NONE', #925 ) ;
#5729=DIRECTION ( 'NONE',  ( -0.000000000000000000, 1.000000000000000000, -0.000000000000000000 ) ) ;
#5734=( CONVERSION_BASED_UNIT ( 'INCH', #1123 ) LENGTH_UNIT ( ) NAMED_UNIT ( #5305 ) );
#5807=ORIENTED_EDGE ( 'NONE', *, *, #5610, .T. ) ;
#5856=EDGE_LOOP ( 'NONE', ( #9060, #8502, #14024, #8446 ) ) ;
#5911=DIRECTION ( 'NONE',  ( -0.000000000000000000, -1.000000000000000000, -0.000000000000000000 ) ) ;
#5926=ORIENTED_EDGE ( 'NONE', *, *, #2912, .T. ) ;
#5932=AXIS2_PLACEMENT_3D ( 'NONE', #3, #14167, #4695 ) ;
#5959=CARTESIAN_POINT ( 'NONE',  ( 0.000000000000000000, 0.000000000000000000, 0.000000000000000000 ) ) ;
#5999=AXIS2_PLACEMENT_3D ( 'NONE', #14349, #7476, #12061 ) ;
#6032=CARTESIAN_POINT ( 'NONE',  ( -0.09035531712817639061, 1.379999999999999671, -0.1564999999999998892 ) ) ;
#6037=CARTESIAN_POINT ( 'NONE',  ( -0.1807106342563527812, 1.379999999999999671, 3.262375646219079751E-17 ) ) ;
#6043=PRODUCT_DEFINITION_SHAPE ( 'NONE', 'NONE',  #2485 ) ;
#6046=DIRECTION ( 'NONE',  ( 0.4999999999999998890, 0.000000000000000000, -0.8660254037844385966 ) ) ;
#6062=EDGE_CURVE ( 'NONE', #13231, #9310, #5590, .T. ) ;
#6075=ORIENTED_EDGE ( 'NONE', *, *, #2600, .T. ) ;
#6089=VECTOR ( 'NONE', #9730, 39.37007874015748854 ) ;
#6122=LINE ( 'NONE', #1205, #14143 ) ;
#6144=DIRECTION ( 'NONE',  ( -0.000000000000000000, -1.000000000000000000, -0.000000000000000000 ) ) ;
#6152=ORIENTED_EDGE ( 'NONE', *, *, #13329, .T. ) ;
#6157=DIRECTION ( 'NONE',  ( -1.000000000000000000, 0.000000000000000000, 0.000000000000000000 ) ) ;
#6164=ORIENTED_EDGE ( 'NONE', *, *, #7176, .F. ) ;
#6180=ADVANCED_FACE ( 'NONE', ( #9569 ), #2598, .F. ) ;
#6184=DIRECTION ( 'NONE',  ( 0.000000000000000000, 0.000000000000000000, -1.000000000000000000 ) ) ;
#6189=DIRECTION ( 'NONE',  ( 0.000000000000000000, 0.000000000000000000, -1.000000000000000000 ) ) ;
#6192=FACE_OUTER_BOUND ( 'NONE', #5856, .T. ) ;
#6238=DIRECTION ( 'NONE',  ( -0.000000000000000000, 1.000000000000000000, -0.000000000000000000 ) ) ;
#6256=DIRECTION ( 'NONE',  ( 0.000000000000000000, 0.000000000000000000, -1.000000000000000000 ) ) ;
#6315=AXIS2_PLACEMENT_3D ( 'NONE', #4218, #3292, #5285 ) ;
#6335=CARTESIAN_POINT ( 'NONE',  ( 0.000000000000000000, 1.629999999999999893, 0.000000000000000000 ) ) ;
#6365=DIRECTION ( 'NONE',  ( 0.000000000000000000, 1.000000000000000000, 0.000000000000000000 ) ) ;
#6388=EDGE_CURVE ( 'NONE', #1017, #10474, #4139, .T. ) ;
#6418=EDGE_CURVE ( 'NONE', #11005, #12302, #6432, .T. ) ;
#6423=EDGE_LOOP ( 'NONE', ( #4526, #11807, #3427, #2355 ) ) ;
#6432=LINE ( 'NONE', #7903, #7441 ) ;
#6518=EDGE_LOOP ( 'NONE', ( #5807, #8928, #599, #6580, #7505, #10733 ) ) ;
#6528=EDGE_CURVE ( 'NONE', #5693, #8959, #3294, .T. ) ;
#6580=ORIENTED_EDGE ( 'NONE', *, *, #6388, .T. ) ;
#6581=DIRECTION ( 'NONE',  ( 0.000000000000000000, 0.000000000000000000, -1.000000000000000000 ) ) ;
#6595=ORIENTED_EDGE ( 'NONE', *, *, #308, .F. ) ;
#6666=DIRECTION ( 'NONE',  ( -0.000000000000000000, 1.000000000000000000, -0.000000000000000000 ) ) ;
#6720=AXIS2_PLACEMENT_3D ( 'NONE', #11496, #4532, #913 ) ;
#6747=EDGE_LOOP ( 'NONE', ( #13514, #11819, #189, #7058 ) ) ;
#6807=( NAMED_UNIT ( * ) SI_UNIT ( $, .STERADIAN. ) SOLID_ANGLE_UNIT ( ) );
#6869=DIRECTION ( 'NONE',  ( 0.000000000000000000, -1.000000000000000000, -0.000000000000000000 ) ) ;
#6871=ORIENTED_EDGE ( 'NONE', *, *, #1182, .T. ) ;
#6877=VECTOR ( 'NONE', #9852, 39.37007874015748143 ) ;
#6882=VERTEX_POINT ( 'NONE', #10163 ) ;
#6936=VECTOR ( 'NONE', #2551, 39.37007874015748143 ) ;
#6960=SHAPE_REPRESENTATION_RELATIONSHIP ( 'NONE' , 'NONE' ,  #8297, #14952 ) ;
#6967=DIRECTION ( 'NONE',  ( 0.000000000000000000, 0.7071067811865491270, 0.7071067811865459074 ) ) ;
#7002=ORIENTED_EDGE ( 'NONE', *, *, #8228, .T. ) ;
#7031=CARTESIAN_POINT ( 'NONE',  ( 0.000000000000000000, 1.159999999999999698, 0.000000000000000000 ) ) ;
#7058=ORIENTED_EDGE ( 'NONE', *, *, #722, .F. ) ;
#7065=CARTESIAN_POINT ( 'NONE',  ( 0.000000000000000000, -1.002374524060224757E-18, 0.000000000000000000 ) ) ;
#7066=CIRCLE ( 'NONE', #2649, 0.1900000000000000577 ) ;
#7129=EDGE_CURVE ( 'NONE', #9822, #9131, #14000, .T. ) ;
#7168=EDGE_LOOP ( 'NONE', ( #9172, #2037, #13298, #2755 ) ) ;
#7176=EDGE_CURVE ( 'NONE', #12880, #8959, #3394, .T. ) ;
#7193=CARTESIAN_POINT ( 'NONE',  ( -0.09035531712817639061, 1.629999999999999893, 0.1565000000000000280 ) ) ;
#7238=CIRCLE ( 'NONE', #9182, 0.2432499999999999385 ) ;
#7264=CIRCLE ( 'NONE', #1611, 0.2812500000000000555 ) ;
#7280=ORIENTED_EDGE ( 'NONE', *, *, #6418, .F. ) ;
#7284=ORIENTED_EDGE ( 'NONE', *, *, #4947, .F. ) ;
#7343=CARTESIAN_POINT ( 'NONE',  ( 0.000000000000000000, 1.591999999999999638, 0.000000000000000000 ) ) ;
#7358=DIRECTION ( 'NONE',  ( 0.000000000000000000, 0.000000000000000000, 1.000000000000000000 ) ) ;
#7385=FACE_OUTER_BOUND ( 'NONE', #6518, .T. ) ;
#7441=VECTOR ( 'NONE', #11421, 39.37007874015748143 ) ;
#7454=ORIENTED_EDGE ( 'NONE', *, *, #13698, .F. ) ;
#7460=CARTESIAN_POINT ( 'NONE',  ( -0.1807106342563527812, 1.629999999999999893, 3.262375646219079751E-17 ) ) ;
#7476=DIRECTION ( 'NONE',  ( -0.8660254037844388186, 0.000000000000000000, 0.4999999999999998335 ) ) ;
#7486=CARTESIAN_POINT ( 'NONE',  ( 0.09035531712817648775, 1.629999999999999893, -0.1564999999999998892 ) ) ;
#7489=CARTESIAN_POINT ( 'NONE',  ( -0.09035531712817639061, 1.379999999999999671, 0.1565000000000000280 ) ) ;
#7505=ORIENTED_EDGE ( 'NONE', *, *, #11281, .T. ) ;
#7554=CARTESIAN_POINT ( 'NONE',  ( 2.326828918379972104E-17, 0.000000000000000000, 0.1900000000000000577 ) ) ;
#7640=CARTESIAN_POINT ( 'NONE',  ( 0.000000000000000000, 1.159999999999999698, -0.1899999999999999745 ) ) ;
#7668=FACE_BOUND ( 'NONE', #14224, .T. ) ;
#7721=CARTESIAN_POINT ( 'NONE',  ( 0.1807106342563528367, 1.379999999999999671, 5.178337979384803075E-18 ) ) ;
#7765=AXIS2_PLACEMENT_3D ( 'NONE', #1241, #8457, #6157 ) ;
#7830=DIRECTION ( 'NONE',  ( 0.4999999999999998890, 0.000000000000000000, -0.8660254037844385966 ) ) ;
#7860=VECTOR ( 'NONE', #11900, 39.37007874015748143 ) ;
#7903=CARTESIAN_POINT ( 'NONE',  ( 0.000000000000000000, 0.000000000000000000, -0.2812500000000000555 ) ) ;
#7922=ORIENTED_EDGE ( 'NONE', *, *, #9186, .F. ) ;
#7925=FACE_OUTER_BOUND ( 'NONE', #1451, .T. ) ;
#7953=VECTOR ( 'NONE', #14685, 39.37007874015748143 ) ;
#8031=CARTESIAN_POINT ( 'NONE',  ( 0.000000000000000000, 1.249999999999999778, 0.000000000000000000 ) ) ;
#8059=CARTESIAN_POINT ( 'NONE',  ( 3.444319122601930972E-17, 1.591999999999999638, 0.2812500000000000555 ) ) ;
#8126=EDGE_CURVE ( 'NONE', #11005, #11602, #7264, .T. ) ;
#8131=CARTESIAN_POINT ( 'NONE',  ( 0.000000000000000000, 0.000000000000000000, 0.000000000000000000 ) ) ;
#8133=DIRECTION ( 'NONE',  ( 0.000000000000000000, 1.000000000000000000, 0.000000000000000000 ) ) ;
#8162=AXIS2_PLACEMENT_3D ( 'NONE', #12702, #9282, #1222 ) ;
#8178=VERTEX_POINT ( 'NONE', #963 ) ;
#8228=EDGE_CURVE ( 'NONE', #10474, #4313, #2356, .T. ) ;
#8292=CARTESIAN_POINT ( 'NONE',  ( -0.09035531712817639061, 1.629999999999999893, 0.1565000000000000280 ) ) ;
#8297=SHAPE_REPRESENTATION ( 'Cap Screw', ( #8424 ), #3278 ) ;
#8330=ADVANCED_FACE ( 'NONE', ( #10544 ), #9481, .T. ) ;
#8343=ORIENTED_EDGE ( 'NONE', *, *, #2912, .F. ) ;
#8352=LINE ( 'NONE', #8489, #1435 ) ;
#8361=ORIENTED_EDGE ( 'NONE', *, *, #12490, .T. ) ;
#8383=LINE ( 'NONE', #9796, #7953 ) ;
#8424=AXIS2_PLACEMENT_3D ( 'NONE', #5062, #7358, #1521 ) ;
#8430=ADVANCED_FACE ( 'NONE', ( #1564 ), #13196, .T. ) ;
#8446=ORIENTED_EDGE ( 'NONE', *, *, #1182, .F. ) ;
#8457=DIRECTION ( 'NONE',  ( -0.000000000000000000, 0.000000000000000000, -1.000000000000000000 ) ) ;
#8479=ORIENTED_EDGE ( 'NONE', *, *, #3401, .F. ) ;
#8489=CARTESIAN_POINT ( 'NONE',  ( 0.09035531712817648775, 1.379999999999999671, -0.1564999999999998892 ) ) ;
#8491=AXIS2_PLACEMENT_3D ( 'NONE', #12207, #1498, #6184 ) ;
#8502=ORIENTED_EDGE ( 'NONE', *, *, #4947, .T. ) ;
#8536=CARTESIAN_POINT ( 'NONE',  ( 0.000000000000000000, 0.000000000000000000, 0.000000000000000000 ) ) ;
#8570=CARTESIAN_POINT ( 'NONE',  ( 1.861463134703978916E-17, -1.002374524060224757E-18, -0.1520000000000001905 ) ) ;
#8577=DIRECTION ( 'NONE',  ( -0.8660254037844387076, 0.000000000000000000, -0.5000000000000001110 ) ) ;
#8588=CARTESIAN_POINT ( 'NONE',  ( 0.000000000000000000, 1.249999999999999778, 0.000000000000000000 ) ) ;
#8635=LINE ( 'NONE', #8570, #14869 ) ;
#8644=PLANE ( 'NONE',  #13619 ) ;
#8677=LINE ( 'NONE', #3721, #2386 ) ;
#8718=DIRECTION ( 'NONE',  ( -0.4999999999999998335, 0.000000000000000000, -0.8660254037844385966 ) ) ;
#8756=AXIS2_PLACEMENT_3D ( 'NONE', #8536, #12036, #10815 ) ;
#8760=CARTESIAN_POINT ( 'NONE',  ( 0.000000000000000000, -1.002374524060224757E-18, 0.000000000000000000 ) ) ;
#8777=FACE_OUTER_BOUND ( 'NONE', #10267, .T. ) ;
#8805=DIRECTION ( 'NONE',  ( -1.000000000000000000, 0.000000000000000000, 0.000000000000000000 ) ) ;
#8820=LENGTH_MEASURE_WITH_UNIT ( LENGTH_MEASURE( 0.02539999999999999897 ), #1916 );
#8861=LINE ( 'NONE', #13500, #12037 ) ;
#8880=VECTOR ( 'NONE', #7830, 39.37007874015748854 ) ;
#8891=( NAMED_UNIT ( * ) SI_UNIT ( $, .STERADIAN. ) SOLID_ANGLE_UNIT ( ) );
#8906=EDGE_CURVE ( 'NONE', #9631, #8918, #8677, .T. ) ;
#8918=VERTEX_POINT ( 'NONE', #7460 ) ;
#8926=DIRECTION ( 'NONE',  ( 0.000000000000000000, 0.000000000000000000, -1.000000000000000000 ) ) ;
#8928=ORIENTED_EDGE ( 'NONE', *, *, #4468, .T. ) ;
#8959=VERTEX_POINT ( 'NONE', #9613 ) ;
#9015=AXIS2_PLACEMENT_3D ( 'NONE', #10198, #13696, #12546 ) ;
#9018=EDGE_CURVE ( 'NONE', #2536, #4313, #14718, .T. ) ;
#9060=ORIENTED_EDGE ( 'NONE', *, *, #14038, .F. ) ;
#9131=VERTEX_POINT ( 'NONE', #9988 ) ;
#9172=ORIENTED_EDGE ( 'NONE', *, *, #13698, .T. ) ;
#9182=AXIS2_PLACEMENT_3D ( 'NONE', #280, #5130, #209 ) ;
#9186=EDGE_CURVE ( 'NONE', #3698, #12880, #139, .T. ) ;
#9233=FACE_BOUND ( 'NONE', #4395, .T. ) ;
#9243=EDGE_CURVE ( 'NONE', #5693, #1017, #10867, .T. ) ;
#9257=FACE_OUTER_BOUND ( 'NONE', #10675, .T. ) ;
#9282=DIRECTION ( 'NONE',  ( -0.000000000000000000, -1.000000000000000000, -0.000000000000000000 ) ) ;
#9299=ORIENTED_EDGE ( 'NONE', *, *, #1136, .T. ) ;
#9310=VERTEX_POINT ( 'NONE', #14375 ) ;
#9440=ADVANCED_FACE ( 'NONE', ( #4433 ), #5432, .F. ) ;
#9441=LINE ( 'NONE', #14085, #13389 ) ;
#9451=EDGE_LOOP ( 'NONE', ( #11013, #13607, #2940, #14397 ) ) ;
#9481=CYLINDRICAL_SURFACE ( 'NONE', #381, 0.1900000000000000577 ) ;
#9493=CARTESIAN_POINT ( 'NONE',  ( 0.1807106342563528367, 1.379999999999999671, 5.178337979384803075E-18 ) ) ;
#9532=( GEOMETRIC_REPRESENTATION_CONTEXT ( 3 ) GLOBAL_UNCERTAINTY_ASSIGNED_CONTEXT ( ( #2490 ) ) GLOBAL_UNIT_ASSIGNED_CONTEXT ( ( #14703, #1838, #8891 ) ) REPRESENTATION_CONTEXT ( 'NONE', 'WORKASPACE' ) );
#9558=EDGE_LOOP ( 'NONE', ( #13758, #712 ) ) ;
#9566=DIRECTION ( 'NONE',  ( -0.5000000000000000000, 0.000000000000000000, 0.8660254037844385966 ) ) ;
#9569=FACE_OUTER_BOUND ( 'NONE', #7168, .T. ) ;
#9613=CARTESIAN_POINT ( 'NONE',  ( 0.1807106342563528367, 1.629999999999999893, 5.178337979384803075E-18 ) ) ;
#9631=VERTEX_POINT ( 'NONE', #6037 ) ;
#9638=ADVANCED_FACE ( 'NONE', ( #4735 ), #1273, .T. ) ;
#9730=DIRECTION ( 'NONE',  ( 0.4999999999999998335, 0.000000000000000000, 0.8660254037844388186 ) ) ;
#9748=CYLINDRICAL_SURFACE ( 'NONE', #8756, 0.3190000000000000058 ) ;
#9762=DIRECTION ( 'NONE',  ( 0.000000000000000000, 1.000000000000000000, 0.000000000000000000 ) ) ;
#9796=CARTESIAN_POINT ( 'NONE',  ( -0.09035531712817639061, 1.379999999999999671, 0.1565000000000000280 ) ) ;
#9820=CARTESIAN_POINT ( 'NONE',  ( -0.1807106342563527812, 1.629999999999999893, 3.262375646219079751E-17 ) ) ;
#9822=VERTEX_POINT ( 'NONE', #5413 ) ;
#9852=DIRECTION ( 'NONE',  ( 1.000000000000000000, 0.000000000000000000, -3.779312718515659280E-16 ) ) ;
#9864=FACE_OUTER_BOUND ( 'NONE', #12299, .T. ) ;
#9892=DIRECTION ( 'NONE',  ( 0.000000000000000000, 1.000000000000000000, 0.000000000000000000 ) ) ;
#9910=CARTESIAN_POINT ( 'NONE',  ( 0.09035531712817647387, 1.629999999999999893, 0.1564999999999999447 ) ) ;
#9919=ORIENTED_EDGE ( 'NONE', *, *, #8906, .T. ) ;
#9988=CARTESIAN_POINT ( 'NONE',  ( 0.000000000000000000, 1.159999999999999698, -0.3190000000000000058 ) ) ;
#10059=ORIENTED_EDGE ( 'NONE', *, *, #12529, .T. ) ;
#10061=LINE ( 'NONE', #10287, #1739 ) ;
#10086=CIRCLE ( 'NONE', #3487, 0.3190000000000000058 ) ;
#10088=CIRCLE ( 'NONE', #13978, 0.1899999999999999745 ) ;
#10089=DIRECTION ( 'NONE',  ( -0.000000000000000000, -1.000000000000000000, -0.000000000000000000 ) ) ;
#10163=CARTESIAN_POINT ( 'NONE',  ( 0.000000000000000000, 1.629999999999999893, -0.2432499999999999385 ) ) ;
#10198=CARTESIAN_POINT ( 'NONE',  ( 0.2812500000000000555, 1.249999999999999778, 0.000000000000000000 ) ) ;
#10209=EDGE_LOOP ( 'NONE', ( #1137, #6152, #2832, #14476 ) ) ;
#10243=CARTESIAN_POINT ( 'NONE',  ( 0.000000000000000000, 1.591999999999999638, 0.000000000000000000 ) ) ;
#10267=EDGE_LOOP ( 'NONE', ( #5926, #8479, #13041, #9919 ) ) ;
#10280=CARTESIAN_POINT ( 'NONE',  ( 0.09035531712817643224, 1.629999999999999893, 0.1564999999999999447 ) ) ;
#10287=CARTESIAN_POINT ( 'NONE',  ( 0.000000000000000000, 0.000000000000000000, -0.3190000000000000058 ) ) ;
#10302=ORIENTED_EDGE ( 'NONE', *, *, #9018, .T. ) ;
#10362=DIRECTION ( 'NONE',  ( 0.000000000000000000, 0.000000000000000000, -1.000000000000000000 ) ) ;
#10368=ORIENTED_EDGE ( 'NONE', *, *, #11010, .F. ) ;
#10419=CARTESIAN_POINT ( 'NONE',  ( 0.09035531712817643224, 1.379999999999999671, 0.1564999999999999447 ) ) ;
#10422=VECTOR ( 'NONE', #5729, 39.37007874015748143 ) ;
#10444=ADVANCED_FACE ( 'NONE', ( #866, #9233 ), #2020, .T. ) ;
#10474=VERTEX_POINT ( 'NONE', #4565 ) ;
#10503=CONICAL_SURFACE ( 'NONE', #3907, 0.1520000000000001905, 0.7853981633974460586 ) ;
#10544=FACE_OUTER_BOUND ( 'NONE', #2415, .T. ) ;
#10594=ORIENTED_EDGE ( 'NONE', *, *, #11281, .F. ) ;
#10666=MANIFOLD_SOLID_BREP ( 'Chamfer1', #13260 ) ;
#10675=EDGE_LOOP ( 'NONE', ( #1538, #5077 ) ) ;
#10680=AXIS2_PLACEMENT_3D ( 'NONE', #734, #14827, #3433 ) ;
#10714=ORIENTED_EDGE ( 'NONE', *, *, #8126, .T. ) ;
#10733=ORIENTED_EDGE ( 'NONE', *, *, #2231, .T. ) ;
#10773=ADVANCED_FACE ( 'NONE', ( #3457 ), #10503, .T. ) ;
#10815=DIRECTION ( 'NONE',  ( 0.000000000000000000, 0.000000000000000000, -1.000000000000000000 ) ) ;
#10851=DIRECTION ( 'NONE',  ( 0.000000000000000000, 0.000000000000000000, -1.000000000000000000 ) ) ;
#10867=LINE ( 'NONE', #7721, #11101 ) ;
#10896=ORIENTED_EDGE ( 'NONE', *, *, #13329, .F. ) ;
#10906=DIRECTION ( 'NONE',  ( 0.000000000000000000, 0.000000000000000000, 1.000000000000000000 ) ) ;
#10945=EDGE_CURVE ( 'NONE', #12302, #2942, #14127, .T. ) ;
#10958=EDGE_LOOP ( 'NONE', ( #11679, #2437 ) ) ;
#10993=DIRECTION ( 'NONE',  ( -0.4999999999999998335, 0.000000000000000000, -0.8660254037844385966 ) ) ;
#11005=VERTEX_POINT ( 'NONE', #662 ) ;
#11010=EDGE_CURVE ( 'NONE', #9310, #5214, #7066, .T. ) ;
#11013=ORIENTED_EDGE ( 'NONE', *, *, #9186, .T. ) ;
#11036=DIRECTION ( 'NONE',  ( 0.4999999999999998335, 0.000000000000000000, 0.8660254037844388186 ) ) ;
#11040=EDGE_LOOP ( 'NONE', ( #1737, #3806, #3885, #2274 ) ) ;
#11041=ORIENTED_EDGE ( 'NONE', *, *, #13034, .F. ) ;
#11083=DIRECTION ( 'NONE',  ( 0.000000000000000000, 0.000000000000000000, -1.000000000000000000 ) ) ;
#11084=CARTESIAN_POINT ( 'NONE',  ( 0.09035531712817648775, 1.379999999999999671, -0.1564999999999998892 ) ) ;
#11101=VECTOR ( 'NONE', #8718, 39.37007874015748854 ) ;
#11108=AXIS2_PLACEMENT_3D ( 'NONE', #5959, #12750, #4817 ) ;
#11120=LINE ( 'NONE', #14646, #12488 ) ;
#11161=AXIS2_PLACEMENT_3D ( 'NONE', #13722, #865, #2185 ) ;
#11220=EDGE_LOOP ( 'NONE', ( #7922, #8343, #14878, #2412, #7454, #6164 ) ) ;
#11223=DIRECTION ( 'NONE',  ( -0.000000000000000000, -1.000000000000000000, -0.000000000000000000 ) ) ;
#11240=PLANE ( 'NONE',  #10680 ) ;
#11256=ORIENTED_EDGE ( 'NONE', *, *, #7129, .F. ) ;
#11281=EDGE_CURVE ( 'NONE', #10474, #9631, #6122, .T. ) ;
#11306=DIRECTION ( 'NONE',  ( -0.000000000000000000, -1.000000000000000000, -0.000000000000000000 ) ) ;
#11368=EDGE_CURVE ( 'NONE', #1017, #2536, #8352, .T. ) ;
#11371=ADVANCED_FACE ( 'NONE', ( #2672 ), #3404, .T. ) ;
#11382=DIRECTION ( 'NONE',  ( -0.000000000000000000, -1.000000000000000000, -0.000000000000000000 ) ) ;
#11384=VERTEX_POINT ( 'NONE', #48 ) ;
#11403=CIRCLE ( 'NONE', #8491, 0.1520000000000001905 ) ;
#11421=DIRECTION ( 'NONE',  ( -0.000000000000000000, -1.000000000000000000, -0.000000000000000000 ) ) ;
#11427=DIRECTION ( 'NONE',  ( -1.000000000000000000, 0.000000000000000000, 0.000000000000000000 ) ) ;
#11437=CIRCLE ( 'NONE', #2414, 0.3190000000000000058 ) ;
#11496=CARTESIAN_POINT ( 'NONE',  ( 0.000000000000000000, 1.591999999999999638, 0.000000000000000000 ) ) ;
#11602=VERTEX_POINT ( 'NONE', #8059 ) ;
#11679=ORIENTED_EDGE ( 'NONE', *, *, #365, .T. ) ;
#11692=ORIENTED_EDGE ( 'NONE', *, *, #722, .T. ) ;
#11711=AXIS2_PLACEMENT_3D ( 'NONE', #7343, #11995, #6189 ) ;
#11723=ORIENTED_EDGE ( 'NONE', *, *, #2600, .F. ) ;
#11761=ADVANCED_FACE ( 'NONE', ( #12810 ), #3661, .T. ) ;
#11771=CARTESIAN_POINT ( 'NONE',  ( 0.000000000000000000, 0.000000000000000000, 0.000000000000000000 ) ) ;
#11774=( NAMED_UNIT ( * ) PLANE_ANGLE_UNIT ( ) SI_UNIT ( $, .RADIAN. ) );
#11807=ORIENTED_EDGE ( 'NONE', *, *, #5161, .T. ) ;
#11819=ORIENTED_EDGE ( 'NONE', *, *, #15034, .F. ) ;
#11873=LINE ( 'NONE', #14231, #6089 ) ;
#11900=DIRECTION ( 'NONE',  ( 8.659560562354915602E-17, -0.7071067811865487940, 0.7071067811865462405 ) ) ;
#11939=DIRECTION ( 'NONE',  ( 1.000000000000000000, 0.000000000000000000, -3.779312718515659280E-16 ) ) ;
#11959=EDGE_LOOP ( 'NONE', ( #11041, #14180 ) ) ;
#11971=VERTEX_POINT ( 'NONE', #13780 ) ;
#11985=CARTESIAN_POINT ( 'NONE',  ( 0.000000000000000000, 1.159999999999999698, 0.000000000000000000 ) ) ;
#11995=DIRECTION ( 'NONE',  ( -0.000000000000000000, -1.000000000000000000, -0.000000000000000000 ) ) ;
#12036=DIRECTION ( 'NONE',  ( -0.000000000000000000, -1.000000000000000000, -0.000000000000000000 ) ) ;
#12037=VECTOR ( 'NONE', #3039, 39.37007874015748854 ) ;
#12061=DIRECTION ( 'NONE',  ( 0.4999999999999998335, 0.000000000000000000, 0.8660254037844388186 ) ) ;
#12069=CARTESIAN_POINT ( 'NONE',  ( 0.000000000000000000, 1.591999999999999638, 0.000000000000000000 ) ) ;
#12091=DIRECTION ( 'NONE',  ( 0.000000000000000000, -0.7071067811865487940, -0.7071067811865462405 ) ) ;
#12152=ORIENTED_EDGE ( 'NONE', *, *, #14359, .T. ) ;
#12172=ORIENTED_EDGE ( 'NONE', *, *, #308, .T. ) ;
#12207=CARTESIAN_POINT ( 'NONE',  ( 0.000000000000000000, -1.002374524060224757E-18, 0.000000000000000000 ) ) ;
#12257=DIRECTION ( 'NONE',  ( 0.000000000000000000, 0.000000000000000000, -1.000000000000000000 ) ) ;
#12298=ORIENTED_EDGE ( 'NONE', *, *, #343, .T. ) ;
#12299=EDGE_LOOP ( 'NONE', ( #12298, #1418, #10594, #7002 ) ) ;
#12302=VERTEX_POINT ( 'NONE', #4233 ) ;
#12378=FACE_BOUND ( 'NONE', #11220, .T. ) ;
#12384=LINE ( 'NONE', #1899, #1567 ) ;
#12392=PRODUCT ( 'Cap Screw', 'Cap Screw', '', ( #14278 ) ) ;
#12465=CARTESIAN_POINT ( 'NONE',  ( 0.1807106342563528367, 1.379999999999999671, 5.178337979384803075E-18 ) ) ;
#12468=CARTESIAN_POINT ( 'NONE',  ( 2.094146026541975510E-17, -1.002374524060224757E-18, -0.1520000000000001905 ) ) ;
#12488=VECTOR ( 'NONE', #13708, 39.37007874015748143 ) ;
#12490=EDGE_CURVE ( 'NONE', #11602, #2942, #5121, .T. ) ;
#12529=EDGE_CURVE ( 'NONE', #2516, #9310, #5257, .T. ) ;
#12536=CIRCLE ( 'NONE', #8162, 0.1520000000000001905 ) ;
#12546=DIRECTION ( 'NONE',  ( 0.000000000000000000, -0.000000000000000000, 1.000000000000000000 ) ) ;
#12561=VECTOR ( 'NONE', #11939, 39.37007874015748143 ) ;
#12658=AXIS2_PLACEMENT_3D ( 'NONE', #438, #14076, #3614 ) ;
#12659=CARTESIAN_POINT ( 'NONE',  ( 0.3190000000000000058, 1.159999999999999698, 0.000000000000000000 ) ) ;
#12669=DIRECTION ( 'NONE',  ( -0.000000000000000000, -1.000000000000000000, -0.000000000000000000 ) ) ;
#12675=DIRECTION ( 'NONE',  ( 0.000000000000000000, 0.000000000000000000, 1.000000000000000000 ) ) ;
#12702=CARTESIAN_POINT ( 'NONE',  ( 0.000000000000000000, -1.002374524060224757E-18, 0.000000000000000000 ) ) ;
#12750=DIRECTION ( 'NONE',  ( -0.000000000000000000, -1.000000000000000000, -0.000000000000000000 ) ) ;
#12810=FACE_OUTER_BOUND ( 'NONE', #6747, .T. ) ;
#12822=EDGE_LOOP ( 'NONE', ( #5018, #9299, #10368, #4256 ) ) ;
#12827=LINE ( 'NONE', #1122, #1863 ) ;
#12880=VERTEX_POINT ( 'NONE', #9910 ) ;
#12907=DIRECTION ( 'NONE',  ( 0.4999999999999998890, 0.000000000000000000, -0.8660254037844385966 ) ) ;
#12961=DIRECTION ( 'NONE',  ( -0.000000000000000000, -1.000000000000000000, -0.000000000000000000 ) ) ;
#12984=DIRECTION ( 'NONE',  ( -0.000000000000000000, 1.000000000000000000, -0.000000000000000000 ) ) ;
#12988=DIRECTION ( 'NONE',  ( 0.8660254037844387076, 0.000000000000000000, -0.4999999999999998890 ) ) ;
#13034=EDGE_CURVE ( 'NONE', #13813, #11971, #3365, .T. ) ;
#13040=DIRECTION ( 'NONE',  ( -0.000000000000000000, -1.000000000000000000, -0.000000000000000000 ) ) ;
#13041=ORIENTED_EDGE ( 'NONE', *, *, #2231, .F. ) ;
#13044=DIRECTION ( 'NONE',  ( -0.000000000000000000, -1.000000000000000000, -0.000000000000000000 ) ) ;
#13099=FACE_OUTER_BOUND ( 'NONE', #6423, .T. ) ;
#13121=DIRECTION ( 'NONE',  ( -0.000000000000000000, -1.000000000000000000, -0.000000000000000000 ) ) ;
#13138=ADVANCED_FACE ( 'NONE', ( #14177 ), #1472, .F. ) ;
#13196=CYLINDRICAL_SURFACE ( 'NONE', #4827, 0.1900000000000000577 ) ;
#13204=CARTESIAN_POINT ( 'NONE',  ( 3.444319122601930972E-17, 0.000000000000000000, 0.2812500000000000555 ) ) ;
#13207=CARTESIAN_POINT ( 'NONE',  ( 0.000000000000000000, 1.159999999999999698, 0.000000000000000000 ) ) ;
#13231=VERTEX_POINT ( 'NONE', #14629 ) ;
#13260=CLOSED_SHELL ( 'NONE', ( #2571, #10773, #8430, #1762, #4711, #4421, #9638, #1928, #15067, #10444, #8330, #1464, #9440, #13707, #4206, #13138, #6180, #219, #2961, #11761, #11371 ) ) ;
#13271=VECTOR ( 'NONE', #6666, 39.37007874015748143 ) ;
#13279=APPLICATION_CONTEXT ( 'automotive_design' ) ;
#13281=DIRECTION ( 'NONE',  ( 8.659560562354913137E-17, 0.7071067811865491270, -0.7071067811865459074 ) ) ;
#13283=ORIENTED_EDGE ( 'NONE', *, *, #5161, .F. ) ;
#13298=ORIENTED_EDGE ( 'NONE', *, *, #9243, .F. ) ;
#13329=EDGE_CURVE ( 'NONE', #11602, #11005, #2320, .T. ) ;
#13354=ORIENTED_EDGE ( 'NONE', *, *, #11010, .T. ) ;
#13369=CIRCLE ( 'NONE', #1380, 0.2812500000000000555 ) ;
#13389=VECTOR ( 'NONE', #12091, 39.37007874015748143 ) ;
#13406=STYLED_ITEM('',(#15199),#10666);
#13420=CARTESIAN_POINT ( 'NONE',  ( 0.000000000000000000, 0.000000000000000000, 0.000000000000000000 ) ) ;
#13500=CARTESIAN_POINT ( 'NONE',  ( -0.09035531712817639061, 1.629999999999999893, -0.1564999999999998892 ) ) ;
#13514=ORIENTED_EDGE ( 'NONE', *, *, #1136, .F. ) ;
#13564=AXIS2_PLACEMENT_3D ( 'NONE', #13207, #2744, #14214 ) ;
#13591=DIRECTION ( 'NONE',  ( 1.000000000000000000, 0.000000000000000000, -3.779312718515659280E-16 ) ) ;
#13607=ORIENTED_EDGE ( 'NONE', *, *, #14689, .F. ) ;
#13619=AXIS2_PLACEMENT_3D ( 'NONE', #5357, #8577, #14515 ) ;
#13671=ORIENTED_EDGE ( 'NONE', *, *, #10945, .T. ) ;
#13674=CARTESIAN_POINT ( 'NONE',  ( -0.09035531712817639061, 1.379999999999999671, 0.1565000000000000280 ) ) ;
#13694=CARTESIAN_POINT ( 'NONE',  ( 0.000000000000000000, 0.03800000000000004763, -0.1900000000000000577 ) ) ;
#13696=DIRECTION ( 'NONE',  ( 0.000000000000000000, 1.000000000000000000, 0.000000000000000000 ) ) ;
#13698=EDGE_CURVE ( 'NONE', #8959, #2536, #12384, .T. ) ;
#13707=ADVANCED_FACE ( 'NONE', ( #8777 ), #1569, .F. ) ;
#13708=DIRECTION ( 'NONE',  ( -0.000000000000000000, -1.000000000000000000, -0.000000000000000000 ) ) ;
#13722=CARTESIAN_POINT ( 'NONE',  ( 0.000000000000000000, 0.000000000000000000, 0.000000000000000000 ) ) ;
#13750=PLANE ( 'NONE',  #6315 ) ;
#13758=ORIENTED_EDGE ( 'NONE', *, *, #15034, .T. ) ;
#13780=CARTESIAN_POINT ( 'NONE',  ( 3.906623289280057325E-17, 1.249999999999999778, 0.3190000000000000058 ) ) ;
#13809=DIRECTION ( 'NONE',  ( 0.000000000000000000, 0.000000000000000000, -1.000000000000000000 ) ) ;
#13813=VERTEX_POINT ( 'NONE', #3154 ) ;
#13920=EDGE_LOOP ( 'NONE', ( #13283, #4503, #14904, #11256 ) ) ;
#13978=AXIS2_PLACEMENT_3D ( 'NONE', #3125, #10089, #4040 ) ;
#14000=CIRCLE ( 'NONE', #4981, 0.3190000000000000058 ) ;
#14024=ORIENTED_EDGE ( 'NONE', *, *, #8126, .F. ) ;
#14038=EDGE_CURVE ( 'NONE', #8178, #6882, #7238, .T. ) ;
#14076=DIRECTION ( 'NONE',  ( -0.000000000000000000, -1.000000000000000000, -0.000000000000000000 ) ) ;
#14085=CARTESIAN_POINT ( 'NONE',  ( 0.000000000000000000, 1.591999999999999638, -0.2812500000000000555 ) ) ;
#14127=CIRCLE ( 'NONE', #12658, 0.2812500000000000555 ) ;
#14142=DIRECTION ( 'NONE',  ( -0.4999999999999998335, 0.000000000000000000, -0.8660254037844385966 ) ) ;
#14143=VECTOR ( 'NONE', #9566, 39.37007874015748854 ) ;
#14167=DIRECTION ( 'NONE',  ( 0.000000000000000000, 1.000000000000000000, 0.000000000000000000 ) ) ;
#14177=FACE_OUTER_BOUND ( 'NONE', #14751, .T. ) ;
#14180=ORIENTED_EDGE ( 'NONE', *, *, #1311, .F. ) ;
#14214=DIRECTION ( 'NONE',  ( 0.000000000000000000, 0.000000000000000000, -1.000000000000000000 ) ) ;
#14224=EDGE_LOOP ( 'NONE', ( #13671, #5231 ) ) ;
#14231=CARTESIAN_POINT ( 'NONE',  ( -0.1807106342563527812, 1.379999999999999671, 3.262375646219079751E-17 ) ) ;
#14278=PRODUCT_CONTEXT ( 'NONE', #13279, 'mechanical' ) ;
#14349=CARTESIAN_POINT ( 'NONE',  ( -0.1807106342563527812, 1.379999999999999671, 3.262375646219079751E-17 ) ) ;
#14359=EDGE_CURVE ( 'NONE', #4201, #5214, #1325, .T. ) ;
#14375=CARTESIAN_POINT ( 'NONE',  ( 2.326828918379972104E-17, 0.03800000000000004763, 0.1900000000000000577 ) ) ;
#14390=DIRECTION ( 'NONE',  ( 0.000000000000000000, 0.000000000000000000, -1.000000000000000000 ) ) ;
#14397=ORIENTED_EDGE ( 'NONE', *, *, #3401, .T. ) ;
#14438=LINE ( 'NONE', #7489, #6877 ) ;
#14476=ORIENTED_EDGE ( 'NONE', *, *, #4401, .F. ) ;
#14515=DIRECTION ( 'NONE',  ( -0.5000000000000000000, 0.000000000000000000, 0.8660254037844385966 ) ) ;
#14520=CARTESIAN_POINT ( 'NONE',  ( 0.000000000000000000, 0.03800000000000004763, 0.000000000000000000 ) ) ;
#14552=DIRECTION ( 'NONE',  ( 0.000000000000000000, -0.000000000000000000, 1.000000000000000000 ) ) ;
#14568=AXIS2_PLACEMENT_3D ( 'NONE', #6335, #5039, #554 ) ;
#14629=CARTESIAN_POINT ( 'NONE',  ( 0.000000000000000000, -1.002374524060224757E-18, 0.1520000000000001905 ) ) ;
#14646=CARTESIAN_POINT ( 'NONE',  ( 3.906623289280057325E-17, 0.000000000000000000, 0.3190000000000000058 ) ) ;
#14685=DIRECTION ( 'NONE',  ( -0.000000000000000000, 1.000000000000000000, -0.000000000000000000 ) ) ;
#14689=EDGE_CURVE ( 'NONE', #15151, #12880, #15016, .T. ) ;
#14693=FACE_OUTER_BOUND ( 'NONE', #9558, .T. ) ;
#14703=( CONVERSION_BASED_UNIT ( 'INCH', #8820 ) LENGTH_UNIT ( ) NAMED_UNIT ( #3938 ) );
#14718=LINE ( 'NONE', #929, #2802 ) ;
#14751=EDGE_LOOP ( 'NONE', ( #10302, #1458, #2732, #4032 ) ) ;
#14827=DIRECTION ( 'NONE',  ( 0.000000000000000000, 1.000000000000000000, 0.000000000000000000 ) ) ;
#14869=VECTOR ( 'NONE', #13281, 39.37007874015748143 ) ;
#14878=ORIENTED_EDGE ( 'NONE', *, *, #343, .F. ) ;
#14886=VERTEX_POINT ( 'NONE', #12468 ) ;
#14904=ORIENTED_EDGE ( 'NONE', *, *, #5210, .T. ) ;
#14952=ADVANCED_BREP_SHAPE_REPRESENTATION ( '', ( #10666, #8424 ), #3278 ) ;
#15016=LINE ( 'NONE', #2479, #6936 ) ;
#15034=EDGE_CURVE ( 'NONE', #13231, #14886, #12536, .T. ) ;
#15059=DIRECTION ( 'NONE',  ( 3.779312718515659280E-16, 0.000000000000000000, 1.000000000000000000 ) ) ;
#15064=CARTESIAN_POINT ( 'NONE',  ( 0.000000000000000000, -1.002374524060224757E-18, 0.1520000000000001905 ) ) ;
#15067=ADVANCED_FACE ( 'NONE', ( #986 ), #3529, .T. ) ;
#15132=DIRECTION ( 'NONE',  ( 0.000000000000000000, 0.000000000000000000, -1.000000000000000000 ) ) ;
#15151=VERTEX_POINT ( 'NONE', #10419 ) ;
#15193=COLOUR_RGB('Black',0.12,0.14,0.17);
#15194=FILL_AREA_STYLE_COLOUR('',#15193);
#15195=FILL_AREA_STYLE('',(#15194));
#15196=SURFACE_STYLE_FILL_AREA(#15195);
#15197=SURFACE_SIDE_STYLE('',(#15196));
#15198=SURFACE_STYLE_USAGE(.BOTH.,#15197);
#15199=PRESENTATION_STYLE_ASSIGNMENT((#15198));
ENDSEC;
END-ISO-10303-21;
